ISO-10303-21;
HEADER;
/* Generated by software containing ST-Developer
 * from STEP Tools, Inc. (www.steptools.com) 
 */

FILE_DESCRIPTION(
/* description */ ('Ball-type isolation valve (generic)'),
/* implementation_level */ '2;1');

FILE_NAME(
/* name */ 'Ball seat (1).step',
/* time_stamp */ '2026-10-27T10:53:05-07:00',
/* author */ (''),
/* organization */ (''),
/* preprocessor_version */ 'ST-DEVELOPER v20.2',
/* originating_system */ 'Autodesk Translation Framework v15.17.0.0',
/* authorisation */ '');

FILE_SCHEMA (('AUTOMOTIVE_DESIGN { 1 0 10303 214 3 1 1 }'));
ENDSEC;

DATA;
#10=MECHANICAL_DESIGN_GEOMETRIC_PRESENTATION_REPRESENTATION('',(#280),#7425);
#228=SHAPE_REPRESENTATION_RELATIONSHIP('SRR','None',#7538,#254);
#254=ADVANCED_BREP_SHAPE_REPRESENTATION('',(#306),#7401);
#280=STYLED_ITEM('',(#7730),#306);
#306=MANIFOLD_SOLID_BREP('Body1',#4085);
#329=SPHERICAL_SURFACE('',#4498,1.5);
#362=FACE_BOUND('',#907,.T.);
#363=FACE_BOUND('',#911,.T.);
#364=FACE_BOUND('',#913,.T.);
#443=PLANE('',#4506);
#444=PLANE('',#4507);
#626=FACE_OUTER_BOUND('',#906,.T.);
#627=FACE_OUTER_BOUND('',#908,.T.);
#628=FACE_OUTER_BOUND('',#909,.T.);
#629=FACE_OUTER_BOUND('',#910,.T.);
#630=FACE_OUTER_BOUND('',#912,.T.);
#906=EDGE_LOOP('',(#2973));
#907=EDGE_LOOP('',(#2974));
#908=EDGE_LOOP('',(#2975,#2976,#2977,#2978));
#909=EDGE_LOOP('',(#2979,#2980,#2981,#2982));
#910=EDGE_LOOP('',(#2983));
#911=EDGE_LOOP('',(#2984));
#912=EDGE_LOOP('',(#2985));
#913=EDGE_LOOP('',(#2986));
#1217=LINE('',#6427,#1525);
#1218=LINE('',#6432,#1526);
#1525=VECTOR('',#5158,0.75);
#1526=VECTOR('',#5163,1.3);
#1828=CIRCLE('',#4499,1.11803398874989);
#1829=CIRCLE('',#4500,0.75);
#1830=CIRCLE('',#4502,0.75);
#1831=CIRCLE('',#4504,1.3);
#1832=CIRCLE('',#4505,1.3);
#2023=VERTEX_POINT('',#6420);
#2024=VERTEX_POINT('',#6422);
#2025=VERTEX_POINT('',#6425);
#2026=VERTEX_POINT('',#6429);
#2027=VERTEX_POINT('',#6431);
#2379=EDGE_CURVE('',#2023,#2023,#1828,.T.);
#2380=EDGE_CURVE('',#2024,#2024,#1829,.T.);
#2381=EDGE_CURVE('',#2025,#2025,#1830,.T.);
#2382=EDGE_CURVE('',#2025,#2024,#1217,.T.);
#2383=EDGE_CURVE('',#2026,#2026,#1831,.T.);
#2384=EDGE_CURVE('',#2026,#2027,#1218,.T.);
#2385=EDGE_CURVE('',#2027,#2027,#1832,.T.);
#2973=ORIENTED_EDGE('',*,*,#2379,.F.);
#2974=ORIENTED_EDGE('',*,*,#2380,.F.);
#2975=ORIENTED_EDGE('',*,*,#2381,.F.);
#2976=ORIENTED_EDGE('',*,*,#2382,.T.);
#2977=ORIENTED_EDGE('',*,*,#2380,.T.);
#2978=ORIENTED_EDGE('',*,*,#2382,.F.);
#2979=ORIENTED_EDGE('',*,*,#2383,.F.);
#2980=ORIENTED_EDGE('',*,*,#2384,.T.);
#2981=ORIENTED_EDGE('',*,*,#2385,.T.);
#2982=ORIENTED_EDGE('',*,*,#2384,.F.);
#2983=ORIENTED_EDGE('',*,*,#2383,.T.);
#2984=ORIENTED_EDGE('',*,*,#2381,.T.);
#2985=ORIENTED_EDGE('',*,*,#2385,.F.);
#2986=ORIENTED_EDGE('',*,*,#2379,.T.);
#3785=CYLINDRICAL_SURFACE('',#4501,0.75);
#3786=CYLINDRICAL_SURFACE('',#4503,1.3);
#3880=ADVANCED_FACE('',(#626,#362),#329,.F.);
#3881=ADVANCED_FACE('',(#627),#3785,.F.);
#3882=ADVANCED_FACE('',(#628),#3786,.T.);
#3883=ADVANCED_FACE('',(#629,#363),#443,.T.);
#3884=ADVANCED_FACE('',(#630,#364),#444,.F.);
#4085=CLOSED_SHELL('',(#3880,#3881,#3882,#3883,#3884));
#4497=AXIS2_PLACEMENT_3D('',#6418,#5146,#5147);
#4498=AXIS2_PLACEMENT_3D('',#6419,#5148,#5149);
#4499=AXIS2_PLACEMENT_3D('',#6421,#5150,#5151);
#4500=AXIS2_PLACEMENT_3D('',#6423,#5152,#5153);
#4501=AXIS2_PLACEMENT_3D('',#6424,#5154,#5155);
#4502=AXIS2_PLACEMENT_3D('',#6426,#5156,#5157);
#4503=AXIS2_PLACEMENT_3D('',#6428,#5159,#5160);
#4504=AXIS2_PLACEMENT_3D('',#6430,#5161,#5162);
#4505=AXIS2_PLACEMENT_3D('',#6433,#5164,#5165);
#4506=AXIS2_PLACEMENT_3D('',#6434,#5166,#5167);
#4507=AXIS2_PLACEMENT_3D('',#6435,#5168,#5169);
#5146=DIRECTION('axis',(0.,0.,1.));
#5147=DIRECTION('refdir',(1.,0.,0.));
#5148=DIRECTION('center_axis',(6.12323399573677E-17,0.,1.));
#5149=DIRECTION('ref_axis',(1.,0.,0.));
#5150=DIRECTION('center_axis',(0.,1.,0.));
#5151=DIRECTION('ref_axis',(0.,0.,1.));
#5152=DIRECTION('center_axis',(0.,-1.,0.));
#5153=DIRECTION('ref_axis',(1.,0.,0.));
#5154=DIRECTION('center_axis',(0.,1.,0.));
#5155=DIRECTION('ref_axis',(1.,0.,0.));
#5156=DIRECTION('center_axis',(0.,-1.,0.));
#5157=DIRECTION('ref_axis',(1.,0.,0.));
#5158=DIRECTION('',(0.,-1.,0.));
#5159=DIRECTION('center_axis',(0.,1.,0.));
#5160=DIRECTION('ref_axis',(1.,0.,0.));
#5161=DIRECTION('center_axis',(0.,1.,0.));
#5162=DIRECTION('ref_axis',(1.,0.,0.));
#5163=DIRECTION('',(0.,-1.,0.));
#5164=DIRECTION('center_axis',(0.,1.,0.));
#5165=DIRECTION('ref_axis',(1.,0.,0.));
#5166=DIRECTION('center_axis',(0.,1.,0.));
#5167=DIRECTION('ref_axis',(1.,0.,0.));
#5168=DIRECTION('center_axis',(0.,1.,0.));
#5169=DIRECTION('ref_axis',(1.,0.,0.));
#6418=CARTESIAN_POINT('',(0.,0.,0.));
#6419=CARTESIAN_POINT('Origin',(0.,0.,5.));
#6420=CARTESIAN_POINT('',(-1.36919674566051E-16,1.,3.88196601125011));
#6421=CARTESIAN_POINT('Origin',(0.,1.,5.));
#6422=CARTESIAN_POINT('',(-0.75,1.29903810567666,5.));
#6423=CARTESIAN_POINT('Origin',(0.,1.29903810567666,5.));
#6424=CARTESIAN_POINT('Origin',(0.,1.,5.));
#6425=CARTESIAN_POINT('',(-0.75,1.8,5.));
#6426=CARTESIAN_POINT('Origin',(0.,1.8,5.));
#6427=CARTESIAN_POINT('',(-0.75,1.,5.));
#6428=CARTESIAN_POINT('Origin',(0.,1.,5.));
#6429=CARTESIAN_POINT('',(-1.3,1.8,5.));
#6430=CARTESIAN_POINT('Origin',(0.,1.8,5.));
#6431=CARTESIAN_POINT('',(-1.3,1.,5.));
#6432=CARTESIAN_POINT('',(-1.3,1.,5.));
#6433=CARTESIAN_POINT('Origin',(0.,1.,5.));
#6434=CARTESIAN_POINT('Origin',(0.,1.8,5.));
#6435=CARTESIAN_POINT('Origin',(0.,1.,5.));
#7371=UNCERTAINTY_MEASURE_WITH_UNIT(LENGTH_MEASURE(0.001),#7426,
'DISTANCE_ACCURACY_VALUE',
'Maximum model space distance between geometric entities at asserted c
onnectivities');
#7395=UNCERTAINTY_MEASURE_WITH_UNIT(LENGTH_MEASURE(0.001),#7426,
'DISTANCE_ACCURACY_VALUE',
'Maximum model space distance between geometric entities at asserted c
onnectivities');
#7401=(
GEOMETRIC_REPRESENTATION_CONTEXT(3)
GLOBAL_UNCERTAINTY_ASSIGNED_CONTEXT((#7371))
GLOBAL_UNIT_ASSIGNED_CONTEXT((#7426,#7428,#7429))
REPRESENTATION_CONTEXT('','3D')
);
#7425=(
GEOMETRIC_REPRESENTATION_CONTEXT(3)
GLOBAL_UNCERTAINTY_ASSIGNED_CONTEXT((#7395))
GLOBAL_UNIT_ASSIGNED_CONTEXT((#7426,#7428,#7429))
REPRESENTATION_CONTEXT('','3D')
);
#7426=(
LENGTH_UNIT()
NAMED_UNIT(*)
SI_UNIT(.CENTI.,.METRE.)
);
#7428=(
NAMED_UNIT(*)
PLANE_ANGLE_UNIT()
SI_UNIT($,.RADIAN.)
);
#7429=(
NAMED_UNIT(*)
SI_UNIT($,.STERADIAN.)
SOLID_ANGLE_UNIT()
);
#7435=SHAPE_DEFINITION_REPRESENTATION(#7464,#7538);
#7464=PRODUCT_DEFINITION_SHAPE('',$,#7568);
#7538=SHAPE_REPRESENTATION('',(#4497),#7401);
#7562=PRODUCT_DEFINITION_CONTEXT('part definition',#7651,'design');
#7568=PRODUCT_DEFINITION('Ball seat (1)','Ball seat (1)',#7597,#7562);
#7597=PRODUCT_DEFINITION_FORMATION('',$,#7658);
#7651=APPLICATION_CONTEXT(
'Core Data for Automotive Mechanical Design Process');
#7652=PRODUCT_CONTEXT('part definition',#7651,'mechanical');
#7658=PRODUCT('Ball seat (1)','Ball seat (1)','Ball seat (1)',(#7652));
#7724=COLOUR_RGB('Light Blue',0.38,0.62,0.78);
#7725=FILL_AREA_STYLE_COLOUR('',#7724);
#7726=FILL_AREA_STYLE('',(#7725));
#7727=SURFACE_STYLE_FILL_AREA(#7726);
#7728=SURFACE_SIDE_STYLE('',(#7727));
#7729=SURFACE_STYLE_USAGE(.BOTH.,#7728);
#7730=PRESENTATION_STYLE_ASSIGNMENT((#7729));
ENDSEC;
END-ISO-10303-21;
